ISO-10303-21;
HEADER;
/* Generated by software containing ST-Developer
 * from STEP Tools, Inc. (www.steptools.com) 
 */

FILE_DESCRIPTION(
/* description */ ('Hand wheel with handle and shaft collar'),
/* implementation_level */ '2;1');

FILE_NAME(
/* name */ 'Bearing cap (1).step',
/* time_stamp */ '2026-10-28T03:23:19-07:00',
/* author */ (''),
/* organization */ (''),
/* preprocessor_version */ 'ST-DEVELOPER v20.2',
/* originating_system */ 'Autodesk Translation Framework v15.17.0.0',
/* authorisation */ '');

FILE_SCHEMA (('AUTOMOTIVE_DESIGN { 1 0 10303 214 3 1 1 }'));
ENDSEC;

DATA;
#10=MECHANICAL_DESIGN_GEOMETRIC_PRESENTATION_REPRESENTATION('',(#401),#10510);
#337=SHAPE_REPRESENTATION_RELATIONSHIP('SRR','None',#10653,#369);
#369=ADVANCED_BREP_SHAPE_REPRESENTATION('',(#448),#10480);
#401=STYLED_ITEM('',(#10908),#448);
#448=MANIFOLD_SOLID_BREP('Body1',#5300);
#525=FACE_BOUND('',#1182,.T.);
#526=FACE_BOUND('',#1186,.T.);
#527=FACE_BOUND('',#1187,.T.);
#528=FACE_BOUND('',#1188,.T.);
#529=FACE_BOUND('',#1189,.T.);
#530=FACE_BOUND('',#1190,.T.);
#531=FACE_BOUND('',#1192,.T.);
#532=FACE_BOUND('',#1193,.T.);
#533=FACE_BOUND('',#1194,.T.);
#534=FACE_BOUND('',#1195,.T.);
#535=FACE_BOUND('',#1196,.T.);
#631=PLANE('',#5820);
#632=PLANE('',#5827);
#633=PLANE('',#5828);
#818=FACE_OUTER_BOUND('',#1176,.T.);
#819=FACE_OUTER_BOUND('',#1177,.T.);
#820=FACE_OUTER_BOUND('',#1178,.T.);
#821=FACE_OUTER_BOUND('',#1179,.T.);
#822=FACE_OUTER_BOUND('',#1180,.T.);
#823=FACE_OUTER_BOUND('',#1181,.T.);
#824=FACE_OUTER_BOUND('',#1183,.T.);
#825=FACE_OUTER_BOUND('',#1184,.T.);
#826=FACE_OUTER_BOUND('',#1185,.T.);
#827=FACE_OUTER_BOUND('',#1191,.T.);
#1176=EDGE_LOOP('',(#3809,#3810,#3811,#3812));
#1177=EDGE_LOOP('',(#3813,#3814,#3815,#3816));
#1178=EDGE_LOOP('',(#3817,#3818,#3819,#3820));
#1179=EDGE_LOOP('',(#3821,#3822,#3823,#3824));
#1180=EDGE_LOOP('',(#3825,#3826,#3827,#3828));
#1181=EDGE_LOOP('',(#3829));
#1182=EDGE_LOOP('',(#3830));
#1183=EDGE_LOOP('',(#3831,#3832,#3833,#3834));
#1184=EDGE_LOOP('',(#3835,#3836,#3837,#3838));
#1185=EDGE_LOOP('',(#3839));
#1186=EDGE_LOOP('',(#3840));
#1187=EDGE_LOOP('',(#3841));
#1188=EDGE_LOOP('',(#3842));
#1189=EDGE_LOOP('',(#3843));
#1190=EDGE_LOOP('',(#3844));
#1191=EDGE_LOOP('',(#3845));
#1192=EDGE_LOOP('',(#3846));
#1193=EDGE_LOOP('',(#3847));
#1194=EDGE_LOOP('',(#3848));
#1195=EDGE_LOOP('',(#3849));
#1196=EDGE_LOOP('',(#3850));
#1595=LINE('',#8451,#1905);
#1596=LINE('',#8457,#1906);
#1597=LINE('',#8463,#1907);
#1598=LINE('',#8469,#1908);
#1599=LINE('',#8475,#1909);
#1600=LINE('',#8483,#1910);
#1601=LINE('',#8488,#1911);
#1905=VECTOR('',#6721,0.225);
#1906=VECTOR('',#6728,0.225);
#1907=VECTOR('',#6735,0.225);
#1908=VECTOR('',#6742,0.225);
#1909=VECTOR('',#6749,1.59);
#1910=VECTOR('',#6760,1.2);
#1911=VECTOR('',#6765,2.4);
#2177=CIRCLE('',#5806,0.225);
#2178=CIRCLE('',#5807,0.225);
#2179=CIRCLE('',#5809,0.225);
#2180=CIRCLE('',#5810,0.225);
#2181=CIRCLE('',#5812,0.225);
#2182=CIRCLE('',#5813,0.225);
#2183=CIRCLE('',#5815,0.225);
#2184=CIRCLE('',#5816,0.225);
#2185=CIRCLE('',#5818,1.59);
#2186=CIRCLE('',#5819,1.59);
#2187=CIRCLE('',#5821,1.2);
#2188=CIRCLE('',#5823,1.2);
#2189=CIRCLE('',#5825,2.4);
#2190=CIRCLE('',#5826,2.4);
#2528=VERTEX_POINT('',#8448);
#2529=VERTEX_POINT('',#8450);
#2530=VERTEX_POINT('',#8454);
#2531=VERTEX_POINT('',#8456);
#2532=VERTEX_POINT('',#8460);
#2533=VERTEX_POINT('',#8462);
#2534=VERTEX_POINT('',#8466);
#2535=VERTEX_POINT('',#8468);
#2536=VERTEX_POINT('',#8472);
#2537=VERTEX_POINT('',#8474);
#2538=VERTEX_POINT('',#8478);
#2539=VERTEX_POINT('',#8481);
#2540=VERTEX_POINT('',#8485);
#2541=VERTEX_POINT('',#8487);
#3022=EDGE_CURVE('',#2528,#2528,#2177,.T.);
#3023=EDGE_CURVE('',#2528,#2529,#1595,.T.);
#3024=EDGE_CURVE('',#2529,#2529,#2178,.T.);
#3025=EDGE_CURVE('',#2530,#2530,#2179,.T.);
#3026=EDGE_CURVE('',#2530,#2531,#1596,.T.);
#3027=EDGE_CURVE('',#2531,#2531,#2180,.T.);
#3028=EDGE_CURVE('',#2532,#2532,#2181,.T.);
#3029=EDGE_CURVE('',#2532,#2533,#1597,.T.);
#3030=EDGE_CURVE('',#2533,#2533,#2182,.T.);
#3031=EDGE_CURVE('',#2534,#2534,#2183,.T.);
#3032=EDGE_CURVE('',#2534,#2535,#1598,.T.);
#3033=EDGE_CURVE('',#2535,#2535,#2184,.T.);
#3034=EDGE_CURVE('',#2536,#2536,#2185,.T.);
#3035=EDGE_CURVE('',#2536,#2537,#1599,.T.);
#3036=EDGE_CURVE('',#2537,#2537,#2186,.T.);
#3037=EDGE_CURVE('',#2538,#2538,#2187,.T.);
#3038=EDGE_CURVE('',#2539,#2539,#2188,.T.);
#3039=EDGE_CURVE('',#2539,#2538,#1600,.T.);
#3040=EDGE_CURVE('',#2540,#2540,#2189,.T.);
#3041=EDGE_CURVE('',#2540,#2541,#1601,.T.);
#3042=EDGE_CURVE('',#2541,#2541,#2190,.T.);
#3809=ORIENTED_EDGE('',*,*,#3022,.F.);
#3810=ORIENTED_EDGE('',*,*,#3023,.T.);
#3811=ORIENTED_EDGE('',*,*,#3024,.F.);
#3812=ORIENTED_EDGE('',*,*,#3023,.F.);
#3813=ORIENTED_EDGE('',*,*,#3025,.F.);
#3814=ORIENTED_EDGE('',*,*,#3026,.T.);
#3815=ORIENTED_EDGE('',*,*,#3027,.F.);
#3816=ORIENTED_EDGE('',*,*,#3026,.F.);
#3817=ORIENTED_EDGE('',*,*,#3028,.F.);
#3818=ORIENTED_EDGE('',*,*,#3029,.T.);
#3819=ORIENTED_EDGE('',*,*,#3030,.F.);
#3820=ORIENTED_EDGE('',*,*,#3029,.F.);
#3821=ORIENTED_EDGE('',*,*,#3031,.F.);
#3822=ORIENTED_EDGE('',*,*,#3032,.T.);
#3823=ORIENTED_EDGE('',*,*,#3033,.F.);
#3824=ORIENTED_EDGE('',*,*,#3032,.F.);
#3825=ORIENTED_EDGE('',*,*,#3034,.F.);
#3826=ORIENTED_EDGE('',*,*,#3035,.T.);
#3827=ORIENTED_EDGE('',*,*,#3036,.T.);
#3828=ORIENTED_EDGE('',*,*,#3035,.F.);
#3829=ORIENTED_EDGE('',*,*,#3036,.F.);
#3830=ORIENTED_EDGE('',*,*,#3037,.F.);
#3831=ORIENTED_EDGE('',*,*,#3038,.F.);
#3832=ORIENTED_EDGE('',*,*,#3039,.T.);
#3833=ORIENTED_EDGE('',*,*,#3037,.T.);
#3834=ORIENTED_EDGE('',*,*,#3039,.F.);
#3835=ORIENTED_EDGE('',*,*,#3040,.F.);
#3836=ORIENTED_EDGE('',*,*,#3041,.T.);
#3837=ORIENTED_EDGE('',*,*,#3042,.T.);
#3838=ORIENTED_EDGE('',*,*,#3041,.F.);
#3839=ORIENTED_EDGE('',*,*,#3040,.T.);
#3840=ORIENTED_EDGE('',*,*,#3038,.T.);
#3841=ORIENTED_EDGE('',*,*,#3033,.T.);
#3842=ORIENTED_EDGE('',*,*,#3030,.T.);
#3843=ORIENTED_EDGE('',*,*,#3027,.T.);
#3844=ORIENTED_EDGE('',*,*,#3024,.T.);
#3845=ORIENTED_EDGE('',*,*,#3042,.F.);
#3846=ORIENTED_EDGE('',*,*,#3034,.T.);
#3847=ORIENTED_EDGE('',*,*,#3031,.T.);
#3848=ORIENTED_EDGE('',*,*,#3028,.T.);
#3849=ORIENTED_EDGE('',*,*,#3025,.T.);
#3850=ORIENTED_EDGE('',*,*,#3022,.T.);
#4901=CYLINDRICAL_SURFACE('',#5805,0.225);
#4902=CYLINDRICAL_SURFACE('',#5808,0.225);
#4903=CYLINDRICAL_SURFACE('',#5811,0.225);
#4904=CYLINDRICAL_SURFACE('',#5814,0.225);
#4905=CYLINDRICAL_SURFACE('',#5817,1.59);
#4906=CYLINDRICAL_SURFACE('',#5822,1.2);
#4907=CYLINDRICAL_SURFACE('',#5824,2.4);
#5030=ADVANCED_FACE('',(#818),#4901,.F.);
#5031=ADVANCED_FACE('',(#819),#4902,.F.);
#5032=ADVANCED_FACE('',(#820),#4903,.F.);
#5033=ADVANCED_FACE('',(#821),#4904,.F.);
#5034=ADVANCED_FACE('',(#822),#4905,.T.);
#5035=ADVANCED_FACE('',(#823,#525),#631,.F.);
#5036=ADVANCED_FACE('',(#824),#4906,.F.);
#5037=ADVANCED_FACE('',(#825),#4907,.T.);
#5038=ADVANCED_FACE('',(#826,#526,#527,#528,#529,#530),#632,.T.);
#5039=ADVANCED_FACE('',(#827,#531,#532,#533,#534,#535),#633,.F.);
#5300=CLOSED_SHELL('',(#5030,#5031,#5032,#5033,#5034,#5035,#5036,#5037,
#5038,#5039));
#5804=AXIS2_PLACEMENT_3D('',#8446,#6715,#6716);
#5805=AXIS2_PLACEMENT_3D('',#8447,#6717,#6718);
#5806=AXIS2_PLACEMENT_3D('',#8449,#6719,#6720);
#5807=AXIS2_PLACEMENT_3D('',#8452,#6722,#6723);
#5808=AXIS2_PLACEMENT_3D('',#8453,#6724,#6725);
#5809=AXIS2_PLACEMENT_3D('',#8455,#6726,#6727);
#5810=AXIS2_PLACEMENT_3D('',#8458,#6729,#6730);
#5811=AXIS2_PLACEMENT_3D('',#8459,#6731,#6732);
#5812=AXIS2_PLACEMENT_3D('',#8461,#6733,#6734);
#5813=AXIS2_PLACEMENT_3D('',#8464,#6736,#6737);
#5814=AXIS2_PLACEMENT_3D('',#8465,#6738,#6739);
#5815=AXIS2_PLACEMENT_3D('',#8467,#6740,#6741);
#5816=AXIS2_PLACEMENT_3D('',#8470,#6743,#6744);
#5817=AXIS2_PLACEMENT_3D('',#8471,#6745,#6746);
#5818=AXIS2_PLACEMENT_3D('',#8473,#6747,#6748);
#5819=AXIS2_PLACEMENT_3D('',#8476,#6750,#6751);
#5820=AXIS2_PLACEMENT_3D('',#8477,#6752,#6753);
#5821=AXIS2_PLACEMENT_3D('',#8479,#6754,#6755);
#5822=AXIS2_PLACEMENT_3D('',#8480,#6756,#6757);
#5823=AXIS2_PLACEMENT_3D('',#8482,#6758,#6759);
#5824=AXIS2_PLACEMENT_3D('',#8484,#6761,#6762);
#5825=AXIS2_PLACEMENT_3D('',#8486,#6763,#6764);
#5826=AXIS2_PLACEMENT_3D('',#8489,#6766,#6767);
#5827=AXIS2_PLACEMENT_3D('',#8490,#6768,#6769);
#5828=AXIS2_PLACEMENT_3D('',#8491,#6770,#6771);
#6715=DIRECTION('axis',(0.,0.,1.));
#6716=DIRECTION('refdir',(1.,0.,0.));
#6717=DIRECTION('center_axis',(0.,1.,0.));
#6718=DIRECTION('ref_axis',(1.,0.,0.));
#6719=DIRECTION('center_axis',(0.,1.,0.));
#6720=DIRECTION('ref_axis',(1.,0.,0.));
#6721=DIRECTION('',(0.,1.,0.));
#6722=DIRECTION('center_axis',(0.,-1.,0.));
#6723=DIRECTION('ref_axis',(1.,0.,0.));
#6724=DIRECTION('center_axis',(0.,1.,0.));
#6725=DIRECTION('ref_axis',(1.,0.,0.));
#6726=DIRECTION('center_axis',(0.,1.,0.));
#6727=DIRECTION('ref_axis',(1.,0.,0.));
#6728=DIRECTION('',(0.,1.,0.));
#6729=DIRECTION('center_axis',(0.,-1.,0.));
#6730=DIRECTION('ref_axis',(1.,0.,0.));
#6731=DIRECTION('center_axis',(0.,1.,0.));
#6732=DIRECTION('ref_axis',(1.,0.,0.));
#6733=DIRECTION('center_axis',(0.,1.,0.));
#6734=DIRECTION('ref_axis',(1.,0.,0.));
#6735=DIRECTION('',(0.,1.,0.));
#6736=DIRECTION('center_axis',(0.,-1.,0.));
#6737=DIRECTION('ref_axis',(1.,0.,0.));
#6738=DIRECTION('center_axis',(0.,1.,0.));
#6739=DIRECTION('ref_axis',(1.,0.,0.));
#6740=DIRECTION('center_axis',(0.,1.,0.));
#6741=DIRECTION('ref_axis',(1.,0.,0.));
#6742=DIRECTION('',(0.,1.,0.));
#6743=DIRECTION('center_axis',(0.,-1.,0.));
#6744=DIRECTION('ref_axis',(1.,0.,0.));
#6745=DIRECTION('center_axis',(0.,1.,0.));
#6746=DIRECTION('ref_axis',(1.,0.,0.));
#6747=DIRECTION('center_axis',(0.,1.,0.));
#6748=DIRECTION('ref_axis',(1.,0.,0.));
#6749=DIRECTION('',(0.,-1.,0.));
#6750=DIRECTION('center_axis',(0.,1.,0.));
#6751=DIRECTION('ref_axis',(1.,0.,0.));
#6752=DIRECTION('center_axis',(0.,1.,0.));
#6753=DIRECTION('ref_axis',(1.,0.,0.));
#6754=DIRECTION('center_axis',(0.,-1.,0.));
#6755=DIRECTION('ref_axis',(1.,0.,0.));
#6756=DIRECTION('center_axis',(0.,1.,0.));
#6757=DIRECTION('ref_axis',(1.,0.,0.));
#6758=DIRECTION('center_axis',(0.,-1.,0.));
#6759=DIRECTION('ref_axis',(1.,0.,0.));
#6760=DIRECTION('',(0.,-1.,0.));
#6761=DIRECTION('center_axis',(0.,1.,0.));
#6762=DIRECTION('ref_axis',(1.,0.,0.));
#6763=DIRECTION('center_axis',(0.,1.,0.));
#6764=DIRECTION('ref_axis',(1.,0.,0.));
#6765=DIRECTION('',(0.,-1.,0.));
#6766=DIRECTION('center_axis',(0.,1.,0.));
#6767=DIRECTION('ref_axis',(1.,0.,0.));
#6768=DIRECTION('center_axis',(0.,1.,0.));
#6769=DIRECTION('ref_axis',(1.,0.,0.));
#6770=DIRECTION('center_axis',(0.,1.,0.));
#6771=DIRECTION('ref_axis',(1.,0.,0.));
#8446=CARTESIAN_POINT('',(0.,0.,0.));
#8447=CARTESIAN_POINT('Origin',(-1.4142135623731,4.4,8.5857864376269));
#8448=CARTESIAN_POINT('',(-1.6392135623731,4.7,8.5857864376269));
#8449=CARTESIAN_POINT('Origin',(-1.4142135623731,4.7,8.5857864376269));
#8450=CARTESIAN_POINT('',(-1.6392135623731,4.9,8.5857864376269));
#8451=CARTESIAN_POINT('',(-1.6392135623731,4.4,8.5857864376269));
#8452=CARTESIAN_POINT('Origin',(-1.4142135623731,4.9,8.5857864376269));
#8453=CARTESIAN_POINT('Origin',(-1.41421356237309,4.4,11.4142135623731));
#8454=CARTESIAN_POINT('',(-1.6392135623731,4.7,11.4142135623731));
#8455=CARTESIAN_POINT('Origin',(-1.41421356237309,4.7,11.4142135623731));
#8456=CARTESIAN_POINT('',(-1.6392135623731,4.9,11.4142135623731));
#8457=CARTESIAN_POINT('',(-1.6392135623731,4.4,11.4142135623731));
#8458=CARTESIAN_POINT('Origin',(-1.41421356237309,4.9,11.4142135623731));
#8459=CARTESIAN_POINT('Origin',(1.4142135623731,4.4,11.4142135623731));
#8460=CARTESIAN_POINT('',(1.1892135623731,4.7,11.4142135623731));
#8461=CARTESIAN_POINT('Origin',(1.4142135623731,4.7,11.4142135623731));
#8462=CARTESIAN_POINT('',(1.1892135623731,4.9,11.4142135623731));
#8463=CARTESIAN_POINT('',(1.1892135623731,4.4,11.4142135623731));
#8464=CARTESIAN_POINT('Origin',(1.4142135623731,4.9,11.4142135623731));
#8465=CARTESIAN_POINT('Origin',(1.41421356237309,4.4,8.5857864376269));
#8466=CARTESIAN_POINT('',(1.18921356237309,4.7,8.5857864376269));
#8467=CARTESIAN_POINT('Origin',(1.41421356237309,4.7,8.5857864376269));
#8468=CARTESIAN_POINT('',(1.18921356237309,4.9,8.5857864376269));
#8469=CARTESIAN_POINT('',(1.18921356237309,4.4,8.5857864376269));
#8470=CARTESIAN_POINT('Origin',(1.41421356237309,4.9,8.5857864376269));
#8471=CARTESIAN_POINT('Origin',(0.,4.5,10.));
#8472=CARTESIAN_POINT('',(-1.59,4.7,10.));
#8473=CARTESIAN_POINT('Origin',(0.,4.7,10.));
#8474=CARTESIAN_POINT('',(-1.59,4.5,10.));
#8475=CARTESIAN_POINT('',(-1.59,4.5,10.));
#8476=CARTESIAN_POINT('Origin',(0.,4.5,10.));
#8477=CARTESIAN_POINT('Origin',(0.,4.5,10.));
#8478=CARTESIAN_POINT('',(-1.2,4.5,10.));
#8479=CARTESIAN_POINT('Origin',(0.,4.5,10.));
#8480=CARTESIAN_POINT('Origin',(0.,4.7,10.));
#8481=CARTESIAN_POINT('',(-1.2,4.9,10.));
#8482=CARTESIAN_POINT('Origin',(0.,4.9,10.));
#8483=CARTESIAN_POINT('',(-1.2,4.7,10.));
#8484=CARTESIAN_POINT('Origin',(0.,4.7,10.));
#8485=CARTESIAN_POINT('',(-2.4,4.9,10.));
#8486=CARTESIAN_POINT('Origin',(0.,4.9,10.));
#8487=CARTESIAN_POINT('',(-2.4,4.7,10.));
#8488=CARTESIAN_POINT('',(-2.4,4.7,10.));
#8489=CARTESIAN_POINT('Origin',(0.,4.7,10.));
#8490=CARTESIAN_POINT('Origin',(0.,4.9,10.));
#8491=CARTESIAN_POINT('Origin',(0.,4.7,10.));
#10441=UNCERTAINTY_MEASURE_WITH_UNIT(LENGTH_MEASURE(0.001),#10511,
'DISTANCE_ACCURACY_VALUE',
'Maximum model space distance between geometric entities at asserted c
onnectivities');
#10471=UNCERTAINTY_MEASURE_WITH_UNIT(LENGTH_MEASURE(0.001),#10511,
'DISTANCE_ACCURACY_VALUE',
'Maximum model space distance between geometric entities at asserted c
onnectivities');
#10480=(
GEOMETRIC_REPRESENTATION_CONTEXT(3)
GLOBAL_UNCERTAINTY_ASSIGNED_CONTEXT((#10441))
GLOBAL_UNIT_ASSIGNED_CONTEXT((#10511,#10513,#10514))
REPRESENTATION_CONTEXT('','3D')
);
#10510=(
GEOMETRIC_REPRESENTATION_CONTEXT(3)
GLOBAL_UNCERTAINTY_ASSIGNED_CONTEXT((#10471))
GLOBAL_UNIT_ASSIGNED_CONTEXT((#10511,#10513,#10514))
REPRESENTATION_CONTEXT('','3D')
);
#10511=(
LENGTH_UNIT()
NAMED_UNIT(*)
SI_UNIT(.CENTI.,.METRE.)
);
#10513=(
NAMED_UNIT(*)
PLANE_ANGLE_UNIT()
SI_UNIT($,.RADIAN.)
);
#10514=(
NAMED_UNIT(*)
SI_UNIT($,.STERADIAN.)
SOLID_ANGLE_UNIT()
);
#10523=SHAPE_DEFINITION_REPRESENTATION(#10561,#10653);
#10561=PRODUCT_DEFINITION_SHAPE('',$,#10692);
#10653=SHAPE_REPRESENTATION('',(#5804),#10480);
#10683=PRODUCT_DEFINITION_CONTEXT('part definition',#10799,'design');
#10692=PRODUCT_DEFINITION('Bearing cap (1)','Bearing cap (1)',#10730,#10683);
#10730=PRODUCT_DEFINITION_FORMATION('',$,#10809);
#10799=APPLICATION_CONTEXT(
'Core Data for Automotive Mechanical Design Process');
#10800=PRODUCT_CONTEXT('part definition',#10799,'mechanical');
#10809=PRODUCT('Bearing cap (1)','Bearing cap (1)','Bearing cap (1)',(#10800));
#10902=COLOUR_RGB('Grey',0.48,0.52,0.57);
#10903=FILL_AREA_STYLE_COLOUR('',#10902);
#10904=FILL_AREA_STYLE('',(#10903));
#10905=SURFACE_STYLE_FILL_AREA(#10904);
#10906=SURFACE_SIDE_STYLE('',(#10905));
#10907=SURFACE_STYLE_USAGE(.BOTH.,#10906);
#10908=PRESENTATION_STYLE_ASSIGNMENT((#10907));
ENDSEC;
END-ISO-10303-21;
